ISO-10303-21;
HEADER;
/* Generated by software containing ST-Developer
 * from STEP Tools, Inc. (www.steptools.com) 
 */

FILE_DESCRIPTION(
/* description */ (''),
/* implementation_level */ '2;1');

FILE_NAME(
/* name */ 'Brass Feed Nut D9 x 15 Lead 2.step',
/* time_stamp */ '2026-10-15T12:29:06-07:00',
/* author */ (''),
/* organization */ (''),
/* preprocessor_version */ 'ST-DEVELOPER v20.2',
/* originating_system */ 'Autodesk Translation Framework v15.15.0.0',
/* authorisation */ '');

FILE_SCHEMA (('AUTOMOTIVE_DESIGN { 1 0 10303 214 3 1 1 }'));
ENDSEC;

DATA;
#10=MECHANICAL_DESIGN_GEOMETRIC_PRESENTATION_REPRESENTATION('',(#1741),#135282);
#1715=SHAPE_REPRESENTATION_RELATIONSHIP('SRR','None',#135339,#1728);
#1728=ADVANCED_BREP_SHAPE_REPRESENTATION('',(#1754),#135271);
#1741=STYLED_ITEM('',(#135413),#1754);
#1754=MANIFOLD_SOLID_BREP('Body1',#32077);
#1784=CYLINDRICAL_SURFACE('',#32389,2.525);
#1785=CYLINDRICAL_SURFACE('',#32400,4.5);
#2032=FACE_BOUND('',#5208,.T.);
#2033=FACE_BOUND('',#5211,.T.);
#2270=PLANE('',#32392);
#2271=PLANE('',#32396);
#3435=FACE_OUTER_BOUND('',#5205,.T.);
#3436=FACE_OUTER_BOUND('',#5206,.T.);
#3437=FACE_OUTER_BOUND('',#5207,.T.);
#3438=FACE_OUTER_BOUND('',#5209,.T.);
#3439=FACE_OUTER_BOUND('',#5210,.T.);
#3440=FACE_OUTER_BOUND('',#5212,.T.);
#3441=FACE_OUTER_BOUND('',#5213,.T.);
#3442=FACE_OUTER_BOUND('',#5214,.T.);
#5205=EDGE_LOOP('',(#21390,#21391,#21392,#21393,#21394));
#5206=EDGE_LOOP('',(#21395,#21396,#21397,#21398,#21399,#21400));
#5207=EDGE_LOOP('',(#21401));
#5208=EDGE_LOOP('',(#21402));
#5209=EDGE_LOOP('',(#21403,#21404,#21405,#21406,#21407));
#5210=EDGE_LOOP('',(#21408));
#5211=EDGE_LOOP('',(#21409));
#5212=EDGE_LOOP('',(#21410,#21411,#21412,#21413));
#5213=EDGE_LOOP('',(#21414,#21415,#21416,#21417));
#5214=EDGE_LOOP('',(#21418,#21419,#21420,#21421));
#7217=LINE('',#41486,#10054);
#7218=LINE('',#41491,#10055);
#7219=LINE('',#41500,#10056);
#7220=LINE('',#41508,#10057);
#7221=LINE('',#41512,#10058);
#7222=LINE('',#41514,#10059);
#10054=VECTOR('',#34681,2.675);
#10055=VECTOR('',#34688,2.525);
#10056=VECTOR('',#34699,2.675);
#10057=VECTOR('',#34710,4.35);
#10058=VECTOR('',#34715,4.5);
#10059=VECTOR('',#34718,4.35);
#12804=CIRCLE('',#32386,2.525);
#12805=CIRCLE('',#32387,2.825);
#12806=CIRCLE('',#32388,2.525);
#12807=CIRCLE('',#32390,2.525);
#12808=CIRCLE('',#32391,2.525);
#12809=CIRCLE('',#32393,4.2);
#12810=CIRCLE('',#32395,2.825);
#12811=CIRCLE('',#32397,4.2);
#12812=CIRCLE('',#32399,4.5);
#12813=CIRCLE('',#32401,4.5);
#13380=VERTEX_POINT('',#41482);
#13381=VERTEX_POINT('',#41483);
#13382=VERTEX_POINT('',#41485);
#13383=VERTEX_POINT('',#41490);
#13384=VERTEX_POINT('',#41492);
#13385=VERTEX_POINT('',#41496);
#13386=VERTEX_POINT('',#41499);
#13387=VERTEX_POINT('',#41503);
#13388=VERTEX_POINT('',#41506);
#13389=VERTEX_POINT('',#41510);
#16546=EDGE_CURVE('',#13380,#13381,#12804,.T.);
#16547=EDGE_CURVE('',#13381,#13382,#7217,.T.);
#16548=EDGE_CURVE('',#13382,#13382,#12805,.T.);
#16549=EDGE_CURVE('',#13381,#13380,#12806,.T.);
#16550=EDGE_CURVE('',#13380,#13383,#7218,.T.);
#16551=EDGE_CURVE('',#13384,#13383,#12807,.T.);
#16552=EDGE_CURVE('',#13383,#13384,#12808,.T.);
#16553=EDGE_CURVE('',#13385,#13385,#12809,.T.);
#16554=EDGE_CURVE('',#13384,#13386,#7219,.T.);
#16555=EDGE_CURVE('',#13386,#13386,#12810,.T.);
#16556=EDGE_CURVE('',#13387,#13387,#12811,.T.);
#16557=EDGE_CURVE('',#13388,#13388,#12812,.T.);
#16558=EDGE_CURVE('',#13388,#13385,#7220,.T.);
#16559=EDGE_CURVE('',#13389,#13389,#12813,.T.);
#16560=EDGE_CURVE('',#13389,#13388,#7221,.T.);
#16561=EDGE_CURVE('',#13389,#13387,#7222,.T.);
#21390=ORIENTED_EDGE('',*,*,#16546,.T.);
#21391=ORIENTED_EDGE('',*,*,#16547,.T.);
#21392=ORIENTED_EDGE('',*,*,#16548,.T.);
#21393=ORIENTED_EDGE('',*,*,#16547,.F.);
#21394=ORIENTED_EDGE('',*,*,#16549,.T.);
#21395=ORIENTED_EDGE('',*,*,#16546,.F.);
#21396=ORIENTED_EDGE('',*,*,#16550,.T.);
#21397=ORIENTED_EDGE('',*,*,#16551,.F.);
#21398=ORIENTED_EDGE('',*,*,#16552,.F.);
#21399=ORIENTED_EDGE('',*,*,#16550,.F.);
#21400=ORIENTED_EDGE('',*,*,#16549,.F.);
#21401=ORIENTED_EDGE('',*,*,#16553,.F.);
#21402=ORIENTED_EDGE('',*,*,#16548,.F.);
#21403=ORIENTED_EDGE('',*,*,#16551,.T.);
#21404=ORIENTED_EDGE('',*,*,#16552,.T.);
#21405=ORIENTED_EDGE('',*,*,#16554,.T.);
#21406=ORIENTED_EDGE('',*,*,#16555,.T.);
#21407=ORIENTED_EDGE('',*,*,#16554,.F.);
#21408=ORIENTED_EDGE('',*,*,#16556,.T.);
#21409=ORIENTED_EDGE('',*,*,#16555,.F.);
#21410=ORIENTED_EDGE('',*,*,#16557,.F.);
#21411=ORIENTED_EDGE('',*,*,#16558,.T.);
#21412=ORIENTED_EDGE('',*,*,#16553,.T.);
#21413=ORIENTED_EDGE('',*,*,#16558,.F.);
#21414=ORIENTED_EDGE('',*,*,#16559,.F.);
#21415=ORIENTED_EDGE('',*,*,#16560,.T.);
#21416=ORIENTED_EDGE('',*,*,#16557,.T.);
#21417=ORIENTED_EDGE('',*,*,#16560,.F.);
#21418=ORIENTED_EDGE('',*,*,#16559,.T.);
#21419=ORIENTED_EDGE('',*,*,#16561,.T.);
#21420=ORIENTED_EDGE('',*,*,#16556,.F.);
#21421=ORIENTED_EDGE('',*,*,#16561,.F.);
#30282=CONICAL_SURFACE('',#32385,2.675,0.785398163397444);
#30283=CONICAL_SURFACE('',#32394,2.675,0.785398163397444);
#30284=CONICAL_SURFACE('',#32398,4.35,0.785398163397459);
#30285=CONICAL_SURFACE('',#32402,4.35,0.785398163397459);
#30410=ADVANCED_FACE('',(#3435),#30282,.F.);
#30411=ADVANCED_FACE('',(#3436),#1784,.F.);
#30412=ADVANCED_FACE('',(#3437,#2032),#2270,.T.);
#30413=ADVANCED_FACE('',(#3438),#30283,.F.);
#30414=ADVANCED_FACE('',(#3439,#2033),#2271,.T.);
#30415=ADVANCED_FACE('',(#3440),#30284,.T.);
#30416=ADVANCED_FACE('',(#3441),#1785,.T.);
#30417=ADVANCED_FACE('',(#3442),#30285,.T.);
#32077=CLOSED_SHELL('',(#30410,#30411,#30412,#30413,#30414,#30415,#30416,
#30417));
#32384=AXIS2_PLACEMENT_3D('',#41480,#34675,#34676);
#32385=AXIS2_PLACEMENT_3D('',#41481,#34677,#34678);
#32386=AXIS2_PLACEMENT_3D('',#41484,#34679,#34680);
#32387=AXIS2_PLACEMENT_3D('',#41487,#34682,#34683);
#32388=AXIS2_PLACEMENT_3D('',#41488,#34684,#34685);
#32389=AXIS2_PLACEMENT_3D('',#41489,#34686,#34687);
#32390=AXIS2_PLACEMENT_3D('',#41493,#34689,#34690);
#32391=AXIS2_PLACEMENT_3D('',#41494,#34691,#34692);
#32392=AXIS2_PLACEMENT_3D('',#41495,#34693,#34694);
#32393=AXIS2_PLACEMENT_3D('',#41497,#34695,#34696);
#32394=AXIS2_PLACEMENT_3D('',#41498,#34697,#34698);
#32395=AXIS2_PLACEMENT_3D('',#41501,#34700,#34701);
#32396=AXIS2_PLACEMENT_3D('',#41502,#34702,#34703);
#32397=AXIS2_PLACEMENT_3D('',#41504,#34704,#34705);
#32398=AXIS2_PLACEMENT_3D('',#41505,#34706,#34707);
#32399=AXIS2_PLACEMENT_3D('',#41507,#34708,#34709);
#32400=AXIS2_PLACEMENT_3D('',#41509,#34711,#34712);
#32401=AXIS2_PLACEMENT_3D('',#41511,#34713,#34714);
#32402=AXIS2_PLACEMENT_3D('',#41513,#34716,#34717);
#34675=DIRECTION('axis',(0.,0.,1.));
#34676=DIRECTION('refdir',(1.,0.,0.));
#34677=DIRECTION('center_axis',(0.,1.,0.));
#34678=DIRECTION('ref_axis',(-1.,0.,0.));
#34679=DIRECTION('center_axis',(0.,-1.,0.));
#34680=DIRECTION('ref_axis',(-1.,0.,0.));
#34681=DIRECTION('',(0.707106781186544,0.707106781186551,-8.6595605623549E-17));
#34682=DIRECTION('center_axis',(0.,1.,0.));
#34683=DIRECTION('ref_axis',(-1.,0.,0.));
#34684=DIRECTION('center_axis',(0.,-1.,0.));
#34685=DIRECTION('ref_axis',(-1.,0.,0.));
#34686=DIRECTION('center_axis',(0.,-1.,0.));
#34687=DIRECTION('ref_axis',(1.,0.,0.));
#34688=DIRECTION('',(0.,-1.,0.));
#34689=DIRECTION('center_axis',(0.,1.,0.));
#34690=DIRECTION('ref_axis',(-1.,0.,0.));
#34691=DIRECTION('center_axis',(0.,1.,0.));
#34692=DIRECTION('ref_axis',(-1.,0.,0.));
#34693=DIRECTION('center_axis',(0.,1.,0.));
#34694=DIRECTION('ref_axis',(0.,0.,1.));
#34695=DIRECTION('center_axis',(0.,-1.,0.));
#34696=DIRECTION('ref_axis',(1.,0.,0.));
#34697=DIRECTION('center_axis',(0.,-1.,0.));
#34698=DIRECTION('ref_axis',(-1.,0.,0.));
#34699=DIRECTION('',(0.707106781186544,-0.707106781186551,8.6595605623549E-17));
#34700=DIRECTION('center_axis',(0.,-1.,0.));
#34701=DIRECTION('ref_axis',(-1.,0.,0.));
#34702=DIRECTION('center_axis',(0.,-1.,0.));
#34703=DIRECTION('ref_axis',(0.,0.,-1.));
#34704=DIRECTION('center_axis',(0.,-1.,0.));
#34705=DIRECTION('ref_axis',(1.,0.,0.));
#34706=DIRECTION('center_axis',(0.,-1.,0.));
#34707=DIRECTION('ref_axis',(1.,0.,0.));
#34708=DIRECTION('center_axis',(0.,-1.,0.));
#34709=DIRECTION('ref_axis',(1.,0.,0.));
#34710=DIRECTION('',(0.707106781186555,0.70710678118654,8.65956056235503E-17));
#34711=DIRECTION('center_axis',(0.,-1.,0.));
#34712=DIRECTION('ref_axis',(1.,0.,0.));
#34713=DIRECTION('center_axis',(0.,-1.,0.));
#34714=DIRECTION('ref_axis',(1.,0.,0.));
#34715=DIRECTION('',(0.,1.,0.));
#34716=DIRECTION('center_axis',(0.,1.,0.));
#34717=DIRECTION('ref_axis',(1.,0.,0.));
#34718=DIRECTION('',(0.707106781186555,-0.70710678118654,-8.65956056235503E-17));
#41480=CARTESIAN_POINT('',(0.,0.,0.));
#41481=CARTESIAN_POINT('Origin',(0.,77.35,13.3));
#41482=CARTESIAN_POINT('',(-2.525,77.2,13.3));
#41483=CARTESIAN_POINT('',(2.52500000000001,77.2,13.3));
#41484=CARTESIAN_POINT('Origin',(0.,77.2,13.3));
#41485=CARTESIAN_POINT('',(2.825,77.5,13.3));
#41486=CARTESIAN_POINT('',(2.675,77.35,13.3));
#41487=CARTESIAN_POINT('Origin',(0.,77.5,13.3));
#41488=CARTESIAN_POINT('Origin',(0.,77.2,13.3));
#41489=CARTESIAN_POINT('Origin',(0.,70.,13.3));
#41490=CARTESIAN_POINT('',(-2.525,62.8,13.3));
#41491=CARTESIAN_POINT('',(-2.525,70.,13.3));
#41492=CARTESIAN_POINT('',(2.525,62.8,13.3));
#41493=CARTESIAN_POINT('Origin',(0.,62.8,13.3));
#41494=CARTESIAN_POINT('Origin',(0.,62.8,13.3));
#41495=CARTESIAN_POINT('Origin',(4.2,77.5,13.3));
#41496=CARTESIAN_POINT('',(-4.2,77.5,13.3));
#41497=CARTESIAN_POINT('Origin',(0.,77.5,13.3));
#41498=CARTESIAN_POINT('Origin',(0.,62.65,13.3));
#41499=CARTESIAN_POINT('',(2.825,62.5,13.3));
#41500=CARTESIAN_POINT('',(2.675,62.65,13.3));
#41501=CARTESIAN_POINT('Origin',(0.,62.5,13.3));
#41502=CARTESIAN_POINT('Origin',(2.525,62.5,13.3));
#41503=CARTESIAN_POINT('',(-4.2,62.5,13.3));
#41504=CARTESIAN_POINT('Origin',(0.,62.5,13.3));
#41505=CARTESIAN_POINT('Origin',(0.,77.35,13.3));
#41506=CARTESIAN_POINT('',(-4.5,77.2,13.3));
#41507=CARTESIAN_POINT('Origin',(0.,77.2,13.3));
#41508=CARTESIAN_POINT('',(-4.35,77.35,13.3));
#41509=CARTESIAN_POINT('Origin',(0.,70.,13.3));
#41510=CARTESIAN_POINT('',(-4.5,62.8,13.3));
#41511=CARTESIAN_POINT('Origin',(0.,62.8,13.3));
#41512=CARTESIAN_POINT('',(-4.5,70.,13.3));
#41513=CARTESIAN_POINT('Origin',(0.,62.65,13.3));
#41514=CARTESIAN_POINT('',(-4.35,62.65,13.3));
#135256=UNCERTAINTY_MEASURE_WITH_UNIT(LENGTH_MEASURE(0.01),#135283,
'DISTANCE_ACCURACY_VALUE',
'Maximum model space distance between geometric entities at asserted c
onnectivities');
#135267=UNCERTAINTY_MEASURE_WITH_UNIT(LENGTH_MEASURE(0.01),#135283,
'DISTANCE_ACCURACY_VALUE',
'Maximum model space distance between geometric entities at asserted c
onnectivities');
#135271=(
GEOMETRIC_REPRESENTATION_CONTEXT(3)
GLOBAL_UNCERTAINTY_ASSIGNED_CONTEXT((#135256))
GLOBAL_UNIT_ASSIGNED_CONTEXT((#135283,#135285,#135286))
REPRESENTATION_CONTEXT('','3D')
);
#135282=(
GEOMETRIC_REPRESENTATION_CONTEXT(3)
GLOBAL_UNCERTAINTY_ASSIGNED_CONTEXT((#135267))
GLOBAL_UNIT_ASSIGNED_CONTEXT((#135283,#135285,#135286))
REPRESENTATION_CONTEXT('','3D')
);
#135283=(
LENGTH_UNIT()
NAMED_UNIT(*)
SI_UNIT(.MILLI.,.METRE.)
);
#135285=(
NAMED_UNIT(*)
PLANE_ANGLE_UNIT()
SI_UNIT($,.RADIAN.)
);
#135286=(
NAMED_UNIT(*)
SI_UNIT($,.STERADIAN.)
SOLID_ANGLE_UNIT()
);
#135290=SHAPE_DEFINITION_REPRESENTATION(#135304,#135339);
#135304=PRODUCT_DEFINITION_SHAPE('',$,#135354);
#135339=SHAPE_REPRESENTATION('',(#32384),#135271);
#135350=PRODUCT_DEFINITION_CONTEXT('part definition',#135394,'design');
#135354=PRODUCT_DEFINITION('2026-10-15-19-09-11-257',
'Brass Feed Nut D9 x 15 Lead 2',#135368,#135350);
#135368=PRODUCT_DEFINITION_FORMATION('',$,#135399);
#135394=APPLICATION_CONTEXT(
'Core Data for Automotive Mechanical Design Process');
#135395=PRODUCT_CONTEXT('part definition',#135394,'mechanical');
#135399=PRODUCT('2026-10-15-19-09-11-257',
'Brass Feed Nut D9 x 15 Lead 2',$,(#135395));
#135413=PRESENTATION_STYLE_ASSIGNMENT((#135427));
#135427=SURFACE_STYLE_USAGE(.BOTH.,#135441);
#135441=SURFACE_SIDE_STYLE('',(#135455));
#135455=SURFACE_STYLE_FILL_AREA(#135469);
#135469=FILL_AREA_STYLE('Opaque(214,178,102)',(#135483));
#135483=FILL_AREA_STYLE_COLOUR('Opaque(214,178,102)',#135497);
#135497=COLOUR_RGB('Opaque(214,178,102)', 0.31764706, 0.68627451, 0.89019608);
ENDSEC;
END-ISO-10303-21;
